ISO-10303-21;
HEADER;
/* Generated by software containing ST-Developer
 * from STEP Tools, Inc. (www.steptools.com) 
 */

FILE_DESCRIPTION(
/* description */ ('Bin tilter linkage'),
/* implementation_level */ '2;1');

FILE_NAME(
/* name */ 'Nut carriage.step',
/* time_stamp */ '2026-10-28T03:26:24-07:00',
/* author */ (''),
/* organization */ (''),
/* preprocessor_version */ 'ST-DEVELOPER v20.2',
/* originating_system */ 'Autodesk Translation Framework v15.17.0.0',
/* authorisation */ '');

FILE_SCHEMA (('AUTOMOTIVE_DESIGN { 1 0 10303 214 3 1 1 }'));
ENDSEC;

DATA;
#10=MECHANICAL_DESIGN_GEOMETRIC_PRESENTATION_REPRESENTATION('',(#960),#23728);
#740=SHAPE_REPRESENTATION_RELATIONSHIP('SRR','None',#24209,#846);
#846=ADVANCED_BREP_SHAPE_REPRESENTATION('',(#1072),#23709);
#960=STYLED_ITEM('',(#24772),#1072);
#1072=MANIFOLD_SOLID_BREP('Body1',#12492);
#1444=FACE_BOUND('',#3690,.T.);
#1445=FACE_BOUND('',#3691,.T.);
#1446=FACE_BOUND('',#3692,.T.);
#1447=FACE_BOUND('',#3695,.T.);
#1448=FACE_BOUND('',#3696,.T.);
#1449=FACE_BOUND('',#3697,.T.);
#1816=PLANE('',#15237);
#1817=PLANE('',#15238);
#1818=PLANE('',#15239);
#1819=PLANE('',#15240);
#1820=PLANE('',#15241);
#1821=PLANE('',#15242);
#2551=FACE_OUTER_BOUND('',#3685,.T.);
#2552=FACE_OUTER_BOUND('',#3686,.T.);
#2553=FACE_OUTER_BOUND('',#3687,.T.);
#2554=FACE_OUTER_BOUND('',#3688,.T.);
#2555=FACE_OUTER_BOUND('',#3689,.T.);
#2556=FACE_OUTER_BOUND('',#3693,.T.);
#2557=FACE_OUTER_BOUND('',#3694,.T.);
#2558=FACE_OUTER_BOUND('',#3698,.T.);
#2559=FACE_OUTER_BOUND('',#3699,.T.);
#3685=EDGE_LOOP('',(#10829,#10830,#10831,#10832));
#3686=EDGE_LOOP('',(#10833,#10834,#10835,#10836));
#3687=EDGE_LOOP('',(#10837,#10838,#10839,#10840));
#3688=EDGE_LOOP('',(#10841,#10842,#10843,#10844));
#3689=EDGE_LOOP('',(#10845,#10846,#10847,#10848));
#3690=EDGE_LOOP('',(#10849));
#3691=EDGE_LOOP('',(#10850));
#3692=EDGE_LOOP('',(#10851));
#3693=EDGE_LOOP('',(#10852,#10853,#10854,#10855));
#3694=EDGE_LOOP('',(#10856,#10857,#10858,#10859));
#3695=EDGE_LOOP('',(#10860));
#3696=EDGE_LOOP('',(#10861));
#3697=EDGE_LOOP('',(#10862));
#3698=EDGE_LOOP('',(#10863,#10864,#10865,#10866));
#3699=EDGE_LOOP('',(#10867,#10868,#10869,#10870));
#4392=LINE('',#22976,#5067);
#4393=LINE('',#22982,#5068);
#4394=LINE('',#22988,#5069);
#4395=LINE('',#22993,#5070);
#4396=LINE('',#22995,#5071);
#4397=LINE('',#22997,#5072);
#4398=LINE('',#22998,#5073);
#4399=LINE('',#23001,#5074);
#4400=LINE('',#23003,#5075);
#4401=LINE('',#23004,#5076);
#4402=LINE('',#23007,#5077);
#4403=LINE('',#23009,#5078);
#4404=LINE('',#23010,#5079);
#4405=LINE('',#23012,#5080);
#4406=LINE('',#23013,#5081);
#5067=VECTOR('',#19125,0.5);
#5068=VECTOR('',#19132,1.05);
#5069=VECTOR('',#19139,1.05);
#5070=VECTOR('',#19144,1.);
#5071=VECTOR('',#19145,1.);
#5072=VECTOR('',#19146,1.);
#5073=VECTOR('',#19147,1.);
#5074=VECTOR('',#19150,1.);
#5075=VECTOR('',#19151,1.);
#5076=VECTOR('',#19152,1.);
#5077=VECTOR('',#19155,1.);
#5078=VECTOR('',#19156,1.);
#5079=VECTOR('',#19157,1.);
#5080=VECTOR('',#19160,1.);
#5081=VECTOR('',#19161,1.);
#5870=CIRCLE('',#15229,0.5);
#5871=CIRCLE('',#15230,0.5);
#5872=CIRCLE('',#15232,1.05);
#5873=CIRCLE('',#15233,1.05);
#5874=CIRCLE('',#15235,1.05);
#5875=CIRCLE('',#15236,1.05);
#6781=VERTEX_POINT('',#22973);
#6782=VERTEX_POINT('',#22975);
#6783=VERTEX_POINT('',#22979);
#6784=VERTEX_POINT('',#22981);
#6785=VERTEX_POINT('',#22985);
#6786=VERTEX_POINT('',#22987);
#6787=VERTEX_POINT('',#22991);
#6788=VERTEX_POINT('',#22992);
#6789=VERTEX_POINT('',#22994);
#6790=VERTEX_POINT('',#22996);
#6791=VERTEX_POINT('',#23000);
#6792=VERTEX_POINT('',#23002);
#6793=VERTEX_POINT('',#23006);
#6794=VERTEX_POINT('',#23008);
#8154=EDGE_CURVE('',#6781,#6781,#5870,.T.);
#8155=EDGE_CURVE('',#6781,#6782,#4392,.T.);
#8156=EDGE_CURVE('',#6782,#6782,#5871,.T.);
#8157=EDGE_CURVE('',#6783,#6783,#5872,.T.);
#8158=EDGE_CURVE('',#6783,#6784,#4393,.T.);
#8159=EDGE_CURVE('',#6784,#6784,#5873,.T.);
#8160=EDGE_CURVE('',#6785,#6785,#5874,.T.);
#8161=EDGE_CURVE('',#6785,#6786,#4394,.T.);
#8162=EDGE_CURVE('',#6786,#6786,#5875,.T.);
#8163=EDGE_CURVE('',#6787,#6788,#4395,.T.);
#8164=EDGE_CURVE('',#6788,#6789,#4396,.T.);
#8165=EDGE_CURVE('',#6790,#6789,#4397,.T.);
#8166=EDGE_CURVE('',#6787,#6790,#4398,.T.);
#8167=EDGE_CURVE('',#6791,#6787,#4399,.T.);
#8168=EDGE_CURVE('',#6792,#6790,#4400,.T.);
#8169=EDGE_CURVE('',#6791,#6792,#4401,.T.);
#8170=EDGE_CURVE('',#6793,#6791,#4402,.T.);
#8171=EDGE_CURVE('',#6794,#6792,#4403,.T.);
#8172=EDGE_CURVE('',#6793,#6794,#4404,.T.);
#8173=EDGE_CURVE('',#6788,#6793,#4405,.T.);
#8174=EDGE_CURVE('',#6789,#6794,#4406,.T.);
#10829=ORIENTED_EDGE('',*,*,#8154,.F.);
#10830=ORIENTED_EDGE('',*,*,#8155,.T.);
#10831=ORIENTED_EDGE('',*,*,#8156,.F.);
#10832=ORIENTED_EDGE('',*,*,#8155,.F.);
#10833=ORIENTED_EDGE('',*,*,#8157,.F.);
#10834=ORIENTED_EDGE('',*,*,#8158,.T.);
#10835=ORIENTED_EDGE('',*,*,#8159,.F.);
#10836=ORIENTED_EDGE('',*,*,#8158,.F.);
#10837=ORIENTED_EDGE('',*,*,#8160,.F.);
#10838=ORIENTED_EDGE('',*,*,#8161,.T.);
#10839=ORIENTED_EDGE('',*,*,#8162,.F.);
#10840=ORIENTED_EDGE('',*,*,#8161,.F.);
#10841=ORIENTED_EDGE('',*,*,#8163,.T.);
#10842=ORIENTED_EDGE('',*,*,#8164,.T.);
#10843=ORIENTED_EDGE('',*,*,#8165,.F.);
#10844=ORIENTED_EDGE('',*,*,#8166,.F.);
#10845=ORIENTED_EDGE('',*,*,#8167,.T.);
#10846=ORIENTED_EDGE('',*,*,#8166,.T.);
#10847=ORIENTED_EDGE('',*,*,#8168,.F.);
#10848=ORIENTED_EDGE('',*,*,#8169,.F.);
#10849=ORIENTED_EDGE('',*,*,#8156,.T.);
#10850=ORIENTED_EDGE('',*,*,#8159,.T.);
#10851=ORIENTED_EDGE('',*,*,#8162,.T.);
#10852=ORIENTED_EDGE('',*,*,#8170,.T.);
#10853=ORIENTED_EDGE('',*,*,#8169,.T.);
#10854=ORIENTED_EDGE('',*,*,#8171,.F.);
#10855=ORIENTED_EDGE('',*,*,#8172,.F.);
#10856=ORIENTED_EDGE('',*,*,#8173,.T.);
#10857=ORIENTED_EDGE('',*,*,#8172,.T.);
#10858=ORIENTED_EDGE('',*,*,#8174,.F.);
#10859=ORIENTED_EDGE('',*,*,#8164,.F.);
#10860=ORIENTED_EDGE('',*,*,#8154,.T.);
#10861=ORIENTED_EDGE('',*,*,#8157,.T.);
#10862=ORIENTED_EDGE('',*,*,#8160,.T.);
#10863=ORIENTED_EDGE('',*,*,#8174,.T.);
#10864=ORIENTED_EDGE('',*,*,#8171,.T.);
#10865=ORIENTED_EDGE('',*,*,#8168,.T.);
#10866=ORIENTED_EDGE('',*,*,#8165,.T.);
#10867=ORIENTED_EDGE('',*,*,#8173,.F.);
#10868=ORIENTED_EDGE('',*,*,#8163,.F.);
#10869=ORIENTED_EDGE('',*,*,#8167,.F.);
#10870=ORIENTED_EDGE('',*,*,#8170,.F.);
#11576=CYLINDRICAL_SURFACE('',#15228,0.5);
#11577=CYLINDRICAL_SURFACE('',#15231,1.05);
#11578=CYLINDRICAL_SURFACE('',#15234,1.05);
#12276=ADVANCED_FACE('',(#2551),#11576,.F.);
#12277=ADVANCED_FACE('',(#2552),#11577,.F.);
#12278=ADVANCED_FACE('',(#2553),#11578,.F.);
#12279=ADVANCED_FACE('',(#2554),#1816,.T.);
#12280=ADVANCED_FACE('',(#2555,#1444,#1445,#1446),#1817,.T.);
#12281=ADVANCED_FACE('',(#2556),#1818,.T.);
#12282=ADVANCED_FACE('',(#2557,#1447,#1448,#1449),#1819,.T.);
#12283=ADVANCED_FACE('',(#2558),#1820,.T.);
#12284=ADVANCED_FACE('',(#2559),#1821,.F.);
#12492=CLOSED_SHELL('',(#12276,#12277,#12278,#12279,#12280,#12281,#12282,
#12283,#12284));
#15227=AXIS2_PLACEMENT_3D('',#22971,#19119,#19120);
#15228=AXIS2_PLACEMENT_3D('',#22972,#19121,#19122);
#15229=AXIS2_PLACEMENT_3D('',#22974,#19123,#19124);
#15230=AXIS2_PLACEMENT_3D('',#22977,#19126,#19127);
#15231=AXIS2_PLACEMENT_3D('',#22978,#19128,#19129);
#15232=AXIS2_PLACEMENT_3D('',#22980,#19130,#19131);
#15233=AXIS2_PLACEMENT_3D('',#22983,#19133,#19134);
#15234=AXIS2_PLACEMENT_3D('',#22984,#19135,#19136);
#15235=AXIS2_PLACEMENT_3D('',#22986,#19137,#19138);
#15236=AXIS2_PLACEMENT_3D('',#22989,#19140,#19141);
#15237=AXIS2_PLACEMENT_3D('',#22990,#19142,#19143);
#15238=AXIS2_PLACEMENT_3D('',#22999,#19148,#19149);
#15239=AXIS2_PLACEMENT_3D('',#23005,#19153,#19154);
#15240=AXIS2_PLACEMENT_3D('',#23011,#19158,#19159);
#15241=AXIS2_PLACEMENT_3D('',#23014,#19162,#19163);
#15242=AXIS2_PLACEMENT_3D('',#23015,#19164,#19165);
#19119=DIRECTION('axis',(0.,0.,1.));
#19120=DIRECTION('refdir',(1.,0.,0.));
#19121=DIRECTION('center_axis',(1.,0.,0.));
#19122=DIRECTION('ref_axis',(0.,0.,-1.));
#19123=DIRECTION('center_axis',(1.,0.,0.));
#19124=DIRECTION('ref_axis',(0.,0.,-1.));
#19125=DIRECTION('',(1.,0.,0.));
#19126=DIRECTION('center_axis',(-1.,0.,0.));
#19127=DIRECTION('ref_axis',(0.,0.,-1.));
#19128=DIRECTION('center_axis',(1.,0.,0.));
#19129=DIRECTION('ref_axis',(0.,0.,-1.));
#19130=DIRECTION('center_axis',(1.,0.,0.));
#19131=DIRECTION('ref_axis',(0.,0.,-1.));
#19132=DIRECTION('',(1.,0.,0.));
#19133=DIRECTION('center_axis',(-1.,0.,0.));
#19134=DIRECTION('ref_axis',(0.,0.,-1.));
#19135=DIRECTION('center_axis',(1.,0.,0.));
#19136=DIRECTION('ref_axis',(0.,0.,-1.));
#19137=DIRECTION('center_axis',(1.,0.,0.));
#19138=DIRECTION('ref_axis',(0.,0.,-1.));
#19139=DIRECTION('',(1.,0.,0.));
#19140=DIRECTION('center_axis',(-1.,0.,0.));
#19141=DIRECTION('ref_axis',(0.,0.,-1.));
#19142=DIRECTION('center_axis',(0.,1.,0.));
#19143=DIRECTION('ref_axis',(-1.,0.,0.));
#19144=DIRECTION('',(-1.,0.,0.));
#19145=DIRECTION('',(0.,0.,1.));
#19146=DIRECTION('',(-1.,0.,0.));
#19147=DIRECTION('',(0.,0.,1.));
#19148=DIRECTION('center_axis',(1.,0.,0.));
#19149=DIRECTION('ref_axis',(0.,1.,0.));
#19150=DIRECTION('',(0.,1.,0.));
#19151=DIRECTION('',(0.,1.,0.));
#19152=DIRECTION('',(0.,0.,1.));
#19153=DIRECTION('center_axis',(0.,-1.,0.));
#19154=DIRECTION('ref_axis',(1.,0.,0.));
#19155=DIRECTION('',(1.,0.,0.));
#19156=DIRECTION('',(1.,0.,0.));
#19157=DIRECTION('',(0.,0.,1.));
#19158=DIRECTION('center_axis',(-1.,0.,0.));
#19159=DIRECTION('ref_axis',(0.,-1.,0.));
#19160=DIRECTION('',(0.,-1.,0.));
#19161=DIRECTION('',(0.,-1.,0.));
#19162=DIRECTION('center_axis',(0.,0.,1.));
#19163=DIRECTION('ref_axis',(1.,0.,0.));
#19164=DIRECTION('center_axis',(0.,0.,1.));
#19165=DIRECTION('ref_axis',(1.,0.,0.));
#22971=CARTESIAN_POINT('',(0.,0.,0.));
#22972=CARTESIAN_POINT('Origin',(-5.8,-4.5,8.));
#22973=CARTESIAN_POINT('',(-5.7,-4.5,8.5));
#22974=CARTESIAN_POINT('Origin',(-5.7,-4.5,8.));
#22975=CARTESIAN_POINT('',(-2.3,-4.5,8.5));
#22976=CARTESIAN_POINT('',(-5.8,-4.5,8.5));
#22977=CARTESIAN_POINT('Origin',(-2.3,-4.5,8.));
#22978=CARTESIAN_POINT('Origin',(-5.8,-7.,8.));
#22979=CARTESIAN_POINT('',(-5.7,-7.,9.05));
#22980=CARTESIAN_POINT('Origin',(-5.7,-7.,8.));
#22981=CARTESIAN_POINT('',(-2.3,-7.,9.05));
#22982=CARTESIAN_POINT('',(-5.8,-7.,9.05));
#22983=CARTESIAN_POINT('Origin',(-2.3,-7.,8.));
#22984=CARTESIAN_POINT('Origin',(-5.8,-2.,8.));
#22985=CARTESIAN_POINT('',(-5.7,-2.,9.05));
#22986=CARTESIAN_POINT('Origin',(-5.7,-2.,8.));
#22987=CARTESIAN_POINT('',(-2.3,-2.,9.05));
#22988=CARTESIAN_POINT('',(-5.8,-2.,9.05));
#22989=CARTESIAN_POINT('Origin',(-2.3,-2.,8.));
#22990=CARTESIAN_POINT('Origin',(-2.3,-0.8,6.3));
#22991=CARTESIAN_POINT('',(-2.3,-0.8,6.3));
#22992=CARTESIAN_POINT('',(-5.7,-0.8,6.3));
#22993=CARTESIAN_POINT('',(-2.3,-0.8,6.3));
#22994=CARTESIAN_POINT('',(-5.7,-0.8,9.7));
#22995=CARTESIAN_POINT('',(-5.7,-0.8,6.3));
#22996=CARTESIAN_POINT('',(-2.3,-0.8,9.7));
#22997=CARTESIAN_POINT('',(-2.3,-0.8,9.7));
#22998=CARTESIAN_POINT('',(-2.3,-0.8,6.3));
#22999=CARTESIAN_POINT('Origin',(-2.3,-8.2,6.3));
#23000=CARTESIAN_POINT('',(-2.3,-8.2,6.3));
#23001=CARTESIAN_POINT('',(-2.3,-8.2,6.3));
#23002=CARTESIAN_POINT('',(-2.3,-8.2,9.7));
#23003=CARTESIAN_POINT('',(-2.3,-8.2,9.7));
#23004=CARTESIAN_POINT('',(-2.3,-8.2,6.3));
#23005=CARTESIAN_POINT('Origin',(-5.7,-8.2,6.3));
#23006=CARTESIAN_POINT('',(-5.7,-8.2,6.3));
#23007=CARTESIAN_POINT('',(-5.7,-8.2,6.3));
#23008=CARTESIAN_POINT('',(-5.7,-8.2,9.7));
#23009=CARTESIAN_POINT('',(-5.7,-8.2,9.7));
#23010=CARTESIAN_POINT('',(-5.7,-8.2,6.3));
#23011=CARTESIAN_POINT('Origin',(-5.7,-0.8,6.3));
#23012=CARTESIAN_POINT('',(-5.7,-0.8,6.3));
#23013=CARTESIAN_POINT('',(-5.7,-0.8,9.7));
#23014=CARTESIAN_POINT('Origin',(-4.,-4.5,9.7));
#23015=CARTESIAN_POINT('Origin',(-4.,-4.5,6.3));
#23592=UNCERTAINTY_MEASURE_WITH_UNIT(LENGTH_MEASURE(0.001),#23729,
'DISTANCE_ACCURACY_VALUE',
'Maximum model space distance between geometric entities at asserted c
onnectivities');
#23611=UNCERTAINTY_MEASURE_WITH_UNIT(LENGTH_MEASURE(0.001),#23729,
'DISTANCE_ACCURACY_VALUE',
'Maximum model space distance between geometric entities at asserted c
onnectivities');
#23709=(
GEOMETRIC_REPRESENTATION_CONTEXT(3)
GLOBAL_UNCERTAINTY_ASSIGNED_CONTEXT((#23592))
GLOBAL_UNIT_ASSIGNED_CONTEXT((#23729,#23731,#23732))
REPRESENTATION_CONTEXT('','3D')
);
#23728=(
GEOMETRIC_REPRESENTATION_CONTEXT(3)
GLOBAL_UNCERTAINTY_ASSIGNED_CONTEXT((#23611))
GLOBAL_UNIT_ASSIGNED_CONTEXT((#23729,#23731,#23732))
REPRESENTATION_CONTEXT('','3D')
);
#23729=(
LENGTH_UNIT()
NAMED_UNIT(*)
SI_UNIT(.CENTI.,.METRE.)
);
#23731=(
NAMED_UNIT(*)
PLANE_ANGLE_UNIT()
SI_UNIT($,.RADIAN.)
);
#23732=(
NAMED_UNIT(*)
SI_UNIT($,.STERADIAN.)
SOLID_ANGLE_UNIT()
);
#23830=SHAPE_DEFINITION_REPRESENTATION(#24068,#24209);
#24068=PRODUCT_DEFINITION_SHAPE('',$,#24326);
#24209=SHAPE_REPRESENTATION('',(#15227),#23709);
#24228=PRODUCT_DEFINITION_CONTEXT('part definition',#24578,'design');
#24326=PRODUCT_DEFINITION('Nut carriage','Nut carriage',#24442,#24228);
#24442=PRODUCT_DEFINITION_FORMATION('',$,#24677);
#24578=APPLICATION_CONTEXT(
'Core Data for Automotive Mechanical Design Process');
#24579=PRODUCT_CONTEXT('part definition',#24578,'mechanical');
#24677=PRODUCT('Nut carriage','Nut carriage','Nut carriage',(#24579));
#24766=COLOUR_RGB('Black',0.12,0.14,0.17);
#24767=FILL_AREA_STYLE_COLOUR('',#24766);
#24768=FILL_AREA_STYLE('',(#24767));
#24769=SURFACE_STYLE_FILL_AREA(#24768);
#24770=SURFACE_SIDE_STYLE('',(#24769));
#24771=SURFACE_STYLE_USAGE(.BOTH.,#24770);
#24772=PRESENTATION_STYLE_ASSIGNMENT((#24771));
ENDSEC;
END-ISO-10303-21;
